ISO-10303-21;
HEADER;
/* Generated by software containing ST-Developer
 * from STEP Tools, Inc. (www.steptools.com) 
 */

FILE_DESCRIPTION(
/* description */ ('PAT-041'),
/* implementation_level */ '2;1');

FILE_NAME(
/* name */ 'Weld-on flange (3).step',
/* time_stamp */ '2026-10-28T22:21:24-07:00',
/* author */ (''),
/* organization */ (''),
/* preprocessor_version */ 'ST-DEVELOPER v20.2',
/* originating_system */ 'Autodesk Translation Framework v15.17.0.0',
/* authorisation */ '');

FILE_SCHEMA (('AUTOMOTIVE_DESIGN { 1 0 10303 214 3 1 1 }'));
ENDSEC;

DATA;
#10=MECHANICAL_DESIGN_GEOMETRIC_PRESENTATION_REPRESENTATION('',(#213),#2507);
#193=SHAPE_REPRESENTATION_RELATIONSHIP('SRR','None',#2578,#203);
#203=ADVANCED_BREP_SHAPE_REPRESENTATION('',(#223),#2501);
#213=STYLED_ITEM('',(#2687),#223);
#223=MANIFOLD_SOLID_BREP('Body1',#1333);
#261=FACE_BOUND('',#451,.T.);
#262=FACE_BOUND('',#452,.T.);
#263=FACE_BOUND('',#453,.T.);
#264=FACE_BOUND('',#454,.T.);
#265=FACE_BOUND('',#455,.T.);
#266=FACE_BOUND('',#457,.T.);
#267=FACE_BOUND('',#458,.T.);
#268=FACE_BOUND('',#459,.T.);
#269=FACE_BOUND('',#460,.T.);
#270=FACE_BOUND('',#461,.T.);
#288=PLANE('',#1542);
#289=PLANE('',#1543);
#341=FACE_OUTER_BOUND('',#444,.T.);
#342=FACE_OUTER_BOUND('',#445,.T.);
#343=FACE_OUTER_BOUND('',#446,.T.);
#344=FACE_OUTER_BOUND('',#447,.T.);
#345=FACE_OUTER_BOUND('',#448,.T.);
#346=FACE_OUTER_BOUND('',#449,.T.);
#347=FACE_OUTER_BOUND('',#450,.T.);
#348=FACE_OUTER_BOUND('',#456,.T.);
#444=EDGE_LOOP('',(#1052,#1053,#1054,#1055));
#445=EDGE_LOOP('',(#1056,#1057,#1058,#1059));
#446=EDGE_LOOP('',(#1060,#1061,#1062,#1063));
#447=EDGE_LOOP('',(#1064,#1065,#1066,#1067));
#448=EDGE_LOOP('',(#1068,#1069,#1070,#1071));
#449=EDGE_LOOP('',(#1072,#1073,#1074,#1075));
#450=EDGE_LOOP('',(#1076));
#451=EDGE_LOOP('',(#1077));
#452=EDGE_LOOP('',(#1078));
#453=EDGE_LOOP('',(#1079));
#454=EDGE_LOOP('',(#1080));
#455=EDGE_LOOP('',(#1081));
#456=EDGE_LOOP('',(#1082));
#457=EDGE_LOOP('',(#1083));
#458=EDGE_LOOP('',(#1084));
#459=EDGE_LOOP('',(#1085));
#460=EDGE_LOOP('',(#1086));
#461=EDGE_LOOP('',(#1087));
#526=LINE('',#2223,#582);
#527=LINE('',#2229,#583);
#528=LINE('',#2235,#584);
#529=LINE('',#2241,#585);
#530=LINE('',#2247,#586);
#531=LINE('',#2253,#587);
#582=VECTOR('',#1815,0.44);
#583=VECTOR('',#1822,0.44);
#584=VECTOR('',#1829,0.44);
#585=VECTOR('',#1836,0.44);
#586=VECTOR('',#1843,1.065);
#587=VECTOR('',#1850,3.5);
#658=CIRCLE('',#1525,0.44);
#659=CIRCLE('',#1526,0.44);
#660=CIRCLE('',#1528,0.44);
#661=CIRCLE('',#1529,0.44);
#662=CIRCLE('',#1531,0.44);
#663=CIRCLE('',#1532,0.44);
#664=CIRCLE('',#1534,0.44);
#665=CIRCLE('',#1535,0.44);
#666=CIRCLE('',#1537,1.065);
#667=CIRCLE('',#1538,1.065);
#668=CIRCLE('',#1540,3.5);
#669=CIRCLE('',#1541,3.5);
#730=VERTEX_POINT('',#2220);
#731=VERTEX_POINT('',#2222);
#732=VERTEX_POINT('',#2226);
#733=VERTEX_POINT('',#2228);
#734=VERTEX_POINT('',#2232);
#735=VERTEX_POINT('',#2234);
#736=VERTEX_POINT('',#2238);
#737=VERTEX_POINT('',#2240);
#738=VERTEX_POINT('',#2244);
#739=VERTEX_POINT('',#2246);
#740=VERTEX_POINT('',#2250);
#741=VERTEX_POINT('',#2252);
#846=EDGE_CURVE('',#730,#730,#658,.T.);
#847=EDGE_CURVE('',#730,#731,#526,.T.);
#848=EDGE_CURVE('',#731,#731,#659,.T.);
#849=EDGE_CURVE('',#732,#732,#660,.T.);
#850=EDGE_CURVE('',#732,#733,#527,.T.);
#851=EDGE_CURVE('',#733,#733,#661,.T.);
#852=EDGE_CURVE('',#734,#734,#662,.T.);
#853=EDGE_CURVE('',#734,#735,#528,.T.);
#854=EDGE_CURVE('',#735,#735,#663,.T.);
#855=EDGE_CURVE('',#736,#736,#664,.T.);
#856=EDGE_CURVE('',#736,#737,#529,.T.);
#857=EDGE_CURVE('',#737,#737,#665,.T.);
#858=EDGE_CURVE('',#738,#738,#666,.T.);
#859=EDGE_CURVE('',#738,#739,#530,.T.);
#860=EDGE_CURVE('',#739,#739,#667,.T.);
#861=EDGE_CURVE('',#740,#740,#668,.T.);
#862=EDGE_CURVE('',#740,#741,#531,.T.);
#863=EDGE_CURVE('',#741,#741,#669,.T.);
#1052=ORIENTED_EDGE('',*,*,#846,.F.);
#1053=ORIENTED_EDGE('',*,*,#847,.T.);
#1054=ORIENTED_EDGE('',*,*,#848,.F.);
#1055=ORIENTED_EDGE('',*,*,#847,.F.);
#1056=ORIENTED_EDGE('',*,*,#849,.F.);
#1057=ORIENTED_EDGE('',*,*,#850,.T.);
#1058=ORIENTED_EDGE('',*,*,#851,.F.);
#1059=ORIENTED_EDGE('',*,*,#850,.F.);
#1060=ORIENTED_EDGE('',*,*,#852,.F.);
#1061=ORIENTED_EDGE('',*,*,#853,.T.);
#1062=ORIENTED_EDGE('',*,*,#854,.F.);
#1063=ORIENTED_EDGE('',*,*,#853,.F.);
#1064=ORIENTED_EDGE('',*,*,#855,.F.);
#1065=ORIENTED_EDGE('',*,*,#856,.T.);
#1066=ORIENTED_EDGE('',*,*,#857,.F.);
#1067=ORIENTED_EDGE('',*,*,#856,.F.);
#1068=ORIENTED_EDGE('',*,*,#858,.F.);
#1069=ORIENTED_EDGE('',*,*,#859,.T.);
#1070=ORIENTED_EDGE('',*,*,#860,.T.);
#1071=ORIENTED_EDGE('',*,*,#859,.F.);
#1072=ORIENTED_EDGE('',*,*,#861,.F.);
#1073=ORIENTED_EDGE('',*,*,#862,.T.);
#1074=ORIENTED_EDGE('',*,*,#863,.T.);
#1075=ORIENTED_EDGE('',*,*,#862,.F.);
#1076=ORIENTED_EDGE('',*,*,#861,.T.);
#1077=ORIENTED_EDGE('',*,*,#858,.T.);
#1078=ORIENTED_EDGE('',*,*,#857,.T.);
#1079=ORIENTED_EDGE('',*,*,#854,.T.);
#1080=ORIENTED_EDGE('',*,*,#851,.T.);
#1081=ORIENTED_EDGE('',*,*,#848,.T.);
#1082=ORIENTED_EDGE('',*,*,#863,.F.);
#1083=ORIENTED_EDGE('',*,*,#860,.F.);
#1084=ORIENTED_EDGE('',*,*,#855,.T.);
#1085=ORIENTED_EDGE('',*,*,#852,.T.);
#1086=ORIENTED_EDGE('',*,*,#849,.T.);
#1087=ORIENTED_EDGE('',*,*,#846,.T.);
#1244=CYLINDRICAL_SURFACE('',#1524,0.44);
#1245=CYLINDRICAL_SURFACE('',#1527,0.44);
#1246=CYLINDRICAL_SURFACE('',#1530,0.44);
#1247=CYLINDRICAL_SURFACE('',#1533,0.44);
#1248=CYLINDRICAL_SURFACE('',#1536,1.065);
#1249=CYLINDRICAL_SURFACE('',#1539,3.5);
#1286=ADVANCED_FACE('',(#341),#1244,.F.);
#1287=ADVANCED_FACE('',(#342),#1245,.F.);
#1288=ADVANCED_FACE('',(#343),#1246,.F.);
#1289=ADVANCED_FACE('',(#344),#1247,.F.);
#1290=ADVANCED_FACE('',(#345),#1248,.F.);
#1291=ADVANCED_FACE('',(#346),#1249,.T.);
#1292=ADVANCED_FACE('',(#347,#261,#262,#263,#264,#265),#288,.T.);
#1293=ADVANCED_FACE('',(#348,#266,#267,#268,#269,#270),#289,.F.);
#1333=CLOSED_SHELL('',(#1286,#1287,#1288,#1289,#1290,#1291,#1292,#1293));
#1523=AXIS2_PLACEMENT_3D('',#2218,#1809,#1810);
#1524=AXIS2_PLACEMENT_3D('',#2219,#1811,#1812);
#1525=AXIS2_PLACEMENT_3D('',#2221,#1813,#1814);
#1526=AXIS2_PLACEMENT_3D('',#2224,#1816,#1817);
#1527=AXIS2_PLACEMENT_3D('',#2225,#1818,#1819);
#1528=AXIS2_PLACEMENT_3D('',#2227,#1820,#1821);
#1529=AXIS2_PLACEMENT_3D('',#2230,#1823,#1824);
#1530=AXIS2_PLACEMENT_3D('',#2231,#1825,#1826);
#1531=AXIS2_PLACEMENT_3D('',#2233,#1827,#1828);
#1532=AXIS2_PLACEMENT_3D('',#2236,#1830,#1831);
#1533=AXIS2_PLACEMENT_3D('',#2237,#1832,#1833);
#1534=AXIS2_PLACEMENT_3D('',#2239,#1834,#1835);
#1535=AXIS2_PLACEMENT_3D('',#2242,#1837,#1838);
#1536=AXIS2_PLACEMENT_3D('',#2243,#1839,#1840);
#1537=AXIS2_PLACEMENT_3D('',#2245,#1841,#1842);
#1538=AXIS2_PLACEMENT_3D('',#2248,#1844,#1845);
#1539=AXIS2_PLACEMENT_3D('',#2249,#1846,#1847);
#1540=AXIS2_PLACEMENT_3D('',#2251,#1848,#1849);
#1541=AXIS2_PLACEMENT_3D('',#2254,#1851,#1852);
#1542=AXIS2_PLACEMENT_3D('',#2255,#1853,#1854);
#1543=AXIS2_PLACEMENT_3D('',#2256,#1855,#1856);
#1809=DIRECTION('axis',(0.,0.,1.));
#1810=DIRECTION('refdir',(1.,0.,0.));
#1811=DIRECTION('center_axis',(1.,0.,0.));
#1812=DIRECTION('ref_axis',(0.,0.,-1.));
#1813=DIRECTION('center_axis',(1.,0.,0.));
#1814=DIRECTION('ref_axis',(0.,0.,-1.));
#1815=DIRECTION('',(1.,0.,0.));
#1816=DIRECTION('center_axis',(-1.,0.,0.));
#1817=DIRECTION('ref_axis',(0.,0.,-1.));
#1818=DIRECTION('center_axis',(1.,0.,0.));
#1819=DIRECTION('ref_axis',(0.,0.,-1.));
#1820=DIRECTION('center_axis',(1.,0.,0.));
#1821=DIRECTION('ref_axis',(0.,0.,-1.));
#1822=DIRECTION('',(1.,0.,0.));
#1823=DIRECTION('center_axis',(-1.,0.,0.));
#1824=DIRECTION('ref_axis',(0.,0.,-1.));
#1825=DIRECTION('center_axis',(1.,0.,0.));
#1826=DIRECTION('ref_axis',(0.,0.,-1.));
#1827=DIRECTION('center_axis',(1.,0.,0.));
#1828=DIRECTION('ref_axis',(0.,0.,-1.));
#1829=DIRECTION('',(1.,0.,0.));
#1830=DIRECTION('center_axis',(-1.,0.,0.));
#1831=DIRECTION('ref_axis',(0.,0.,-1.));
#1832=DIRECTION('center_axis',(1.,0.,0.));
#1833=DIRECTION('ref_axis',(0.,0.,-1.));
#1834=DIRECTION('center_axis',(1.,0.,0.));
#1835=DIRECTION('ref_axis',(0.,0.,-1.));
#1836=DIRECTION('',(1.,0.,0.));
#1837=DIRECTION('center_axis',(-1.,0.,0.));
#1838=DIRECTION('ref_axis',(0.,0.,-1.));
#1839=DIRECTION('center_axis',(1.,0.,0.));
#1840=DIRECTION('ref_axis',(0.,0.,-1.));
#1841=DIRECTION('center_axis',(-1.,0.,0.));
#1842=DIRECTION('ref_axis',(0.,0.,-1.));
#1843=DIRECTION('',(-1.,0.,0.));
#1844=DIRECTION('center_axis',(-1.,0.,0.));
#1845=DIRECTION('ref_axis',(0.,0.,-1.));
#1846=DIRECTION('center_axis',(1.,0.,0.));
#1847=DIRECTION('ref_axis',(0.,0.,-1.));
#1848=DIRECTION('center_axis',(1.,0.,0.));
#1849=DIRECTION('ref_axis',(0.,0.,-1.));
#1850=DIRECTION('',(-1.,0.,0.));
#1851=DIRECTION('center_axis',(1.,0.,0.));
#1852=DIRECTION('ref_axis',(0.,0.,-1.));
#1853=DIRECTION('center_axis',(1.,0.,0.));
#1854=DIRECTION('ref_axis',(0.,0.,-1.));
#1855=DIRECTION('center_axis',(1.,0.,0.));
#1856=DIRECTION('ref_axis',(0.,0.,-1.));
#2218=CARTESIAN_POINT('',(0.,0.,0.));
#2219=CARTESIAN_POINT('Origin',(10.1,-1.90918830920368,-1.90918830920368));
#2220=CARTESIAN_POINT('',(10.2,-1.90918830920368,-1.46918830920368));
#2221=CARTESIAN_POINT('Origin',(10.2,-1.90918830920368,-1.90918830920368));
#2222=CARTESIAN_POINT('',(11.,-1.90918830920368,-1.46918830920368));
#2223=CARTESIAN_POINT('',(10.1,-1.90918830920368,-1.46918830920368));
#2224=CARTESIAN_POINT('Origin',(11.,-1.90918830920368,-1.90918830920368));
#2225=CARTESIAN_POINT('Origin',(10.1,-1.90918830920368,1.90918830920368));
#2226=CARTESIAN_POINT('',(10.2,-1.90918830920368,2.34918830920368));
#2227=CARTESIAN_POINT('Origin',(10.2,-1.90918830920368,1.90918830920368));
#2228=CARTESIAN_POINT('',(11.,-1.90918830920368,2.34918830920368));
#2229=CARTESIAN_POINT('',(10.1,-1.90918830920368,2.34918830920368));
#2230=CARTESIAN_POINT('Origin',(11.,-1.90918830920368,1.90918830920368));
#2231=CARTESIAN_POINT('Origin',(10.1,1.90918830920368,1.90918830920368));
#2232=CARTESIAN_POINT('',(10.2,1.90918830920368,2.34918830920368));
#2233=CARTESIAN_POINT('Origin',(10.2,1.90918830920368,1.90918830920368));
#2234=CARTESIAN_POINT('',(11.,1.90918830920368,2.34918830920368));
#2235=CARTESIAN_POINT('',(10.1,1.90918830920368,2.34918830920368));
#2236=CARTESIAN_POINT('Origin',(11.,1.90918830920368,1.90918830920368));
#2237=CARTESIAN_POINT('Origin',(10.1,1.90918830920368,-1.90918830920368));
#2238=CARTESIAN_POINT('',(10.2,1.90918830920368,-1.46918830920368));
#2239=CARTESIAN_POINT('Origin',(10.2,1.90918830920368,-1.90918830920368));
#2240=CARTESIAN_POINT('',(11.,1.90918830920368,-1.46918830920368));
#2241=CARTESIAN_POINT('',(10.1,1.90918830920368,-1.46918830920368));
#2242=CARTESIAN_POINT('Origin',(11.,1.90918830920368,-1.90918830920368));
#2243=CARTESIAN_POINT('Origin',(10.2,0.,0.));
#2244=CARTESIAN_POINT('',(11.,-1.30424884109193E-16,1.065));
#2245=CARTESIAN_POINT('Origin',(11.,0.,0.));
#2246=CARTESIAN_POINT('',(10.2,-1.30424884109193E-16,1.065));
#2247=CARTESIAN_POINT('',(10.2,-1.30424884109193E-16,1.065));
#2248=CARTESIAN_POINT('Origin',(10.2,0.,0.));
#2249=CARTESIAN_POINT('Origin',(10.2,0.,0.));
#2250=CARTESIAN_POINT('',(11.,-4.28626379701574E-16,3.5));
#2251=CARTESIAN_POINT('Origin',(11.,0.,0.));
#2252=CARTESIAN_POINT('',(10.2,-4.28626379701574E-16,3.5));
#2253=CARTESIAN_POINT('',(10.2,-4.28626379701574E-16,3.5));
#2254=CARTESIAN_POINT('Origin',(10.2,0.,0.));
#2255=CARTESIAN_POINT('Origin',(11.,0.,0.));
#2256=CARTESIAN_POINT('Origin',(10.2,0.,0.));
#2489=UNCERTAINTY_MEASURE_WITH_UNIT(LENGTH_MEASURE(0.001),#2508,
'DISTANCE_ACCURACY_VALUE',
'Maximum model space distance between geometric entities at asserted c
onnectivities');
#2495=UNCERTAINTY_MEASURE_WITH_UNIT(LENGTH_MEASURE(0.001),#2508,
'DISTANCE_ACCURACY_VALUE',
'Maximum model space distance between geometric entities at asserted c
onnectivities');
#2501=(
GEOMETRIC_REPRESENTATION_CONTEXT(3)
GLOBAL_UNCERTAINTY_ASSIGNED_CONTEXT((#2489))
GLOBAL_UNIT_ASSIGNED_CONTEXT((#2508,#2510,#2511))
REPRESENTATION_CONTEXT('','3D')
);
#2507=(
GEOMETRIC_REPRESENTATION_CONTEXT(3)
GLOBAL_UNCERTAINTY_ASSIGNED_CONTEXT((#2495))
GLOBAL_UNIT_ASSIGNED_CONTEXT((#2508,#2510,#2511))
REPRESENTATION_CONTEXT('','3D')
);
#2508=(
LENGTH_UNIT()
NAMED_UNIT(*)
SI_UNIT(.CENTI.,.METRE.)
);
#2510=(
NAMED_UNIT(*)
PLANE_ANGLE_UNIT()
SI_UNIT($,.RADIAN.)
);
#2511=(
NAMED_UNIT(*)
SI_UNIT($,.STERADIAN.)
SOLID_ANGLE_UNIT()
);
#2517=SHAPE_DEFINITION_REPRESENTATION(#2528,#2578);
#2528=PRODUCT_DEFINITION_SHAPE('',$,#2590);
#2578=SHAPE_REPRESENTATION('',(#1523),#2501);
#2584=PRODUCT_DEFINITION_CONTEXT('part definition',#2619,'design');
#2590=PRODUCT_DEFINITION('Weld-on flange (3)',
'Weld-on flange (3)',#2601,#2584);
#2601=PRODUCT_DEFINITION_FORMATION('',$,#2626);
#2619=APPLICATION_CONTEXT(
'Core Data for Automotive Mechanical Design Process');
#2620=PRODUCT_CONTEXT('part definition',#2619,'mechanical');
#2626=PRODUCT('Weld-on flange (3)','Weld-on flange (3)',
'Weld-on flange (3)',(#2620));
#2681=COLOUR_RGB('Sky Blue',0.24,0.69,0.87);
#2682=FILL_AREA_STYLE_COLOUR('',#2681);
#2683=FILL_AREA_STYLE('',(#2682));
#2684=SURFACE_STYLE_FILL_AREA(#2683);
#2685=SURFACE_SIDE_STYLE('',(#2684));
#2686=SURFACE_STYLE_USAGE(.BOTH.,#2685);
#2687=PRESENTATION_STYLE_ASSIGNMENT((#2686));
ENDSEC;
END-ISO-10303-21;
